ISO-10303-21;
HEADER;
FILE_DESCRIPTION (('STEP AP203'),
    '1' );
FILE_NAME ('1602p_c_25.step',
    '2026-10-31T14:11:27',
    ( '' ),
    ( '' ),
    'SwSTEP 2.0',
    'SolidWorks 2024',
    '' );
FILE_SCHEMA (( 'AUTOMOTIVE_DESIGN' ));
ENDSEC;

DATA;
#52=DIRECTION ( 'NONE',  ( 0.9999862922474493931, 0.005235963827110273229, 0.000000000000000000 ) ) ;
#58=DIRECTION ( 'NONE',  ( -0.9999862922474493931, -0.005235963827110211646, -9.568357752077023983E-37 ) ) ;
#415=DIRECTION ( 'NONE',  ( 1.000000000000000000, 0.000000000000000000, 0.000000000000000000 ) ) ;
#567=ADVANCED_BREP_SHAPE_REPRESENTATION ( '', ( #1705, #12739 ), #22737 ) ;
#1206=ADVANCED_FACE ( 'NONE', ( #18463 ), #9683, .T. ) ;
#1338=CARTESIAN_POINT ( 'NONE',  ( -62.84171802989940403, -5.847508446296020068, -7.200000000000000178 ) ) ;
#1392=VECTOR ( 'NONE', #14982, 1000.000000000000000 ) ;
#1586=VECTOR ( 'NONE', #21926, 1000.000000000000000 ) ;
#1637=VERTEX_POINT ( 'NONE', #12289 ) ;
#1705=MANIFOLD_SOLID_BREP ( 'Boss-Extrude2', #10594 ) ;
#1719=FACE_OUTER_BOUND ( 'NONE', #13019, .T. ) ;
#1752=ORIENTED_EDGE ( 'NONE', *, *, #8865, .F. ) ;
#1883=PRODUCT ( '1602p_c_25', '1602p_c_25', '', ( #13536 ) ) ;
#1909=( NAMED_UNIT ( * ) PLANE_ANGLE_UNIT ( ) SI_UNIT ( $, .RADIAN. ) );
#2122=EDGE_CURVE ( 'NONE', #23060, #1637, #19708, .T. ) ;
#2338=CARTESIAN_POINT ( 'NONE',  ( -69.91240388362392366, 7.634045827809349483, 7.200000000000000178 ) ) ;
#2363=VECTOR ( 'NONE', #13809, 1000.000000000000000 ) ;
#2396=( LENGTH_UNIT ( ) NAMED_UNIT ( * ) SI_UNIT ( .MILLI., .METRE. ) );
#2569=CARTESIAN_POINT ( 'NONE',  ( 0.000000000000000000, 0.000000000000000000, 0.000000000000000000 ) ) ;
#3062=AXIS2_PLACEMENT_3D ( 'NONE', #12486, #14369, #18055 ) ;
#3067=ORIENTED_EDGE ( 'NONE', *, *, #18695, .T. ) ;
#3081=SHAPE_DEFINITION_REPRESENTATION ( #12139, #11914 ) ;
#3159=LINE ( 'NONE', #10428, #16604 ) ;
#3209=DIRECTION ( 'NONE',  ( -0.005235963827110212514, 0.9999862922474493931, -1.836993535195700665E-15 ) ) ;
#3218=ORIENTED_EDGE ( 'NONE', *, *, #4848, .F. ) ;
#3248=DIRECTION ( 'NONE',  ( 0.000000000000000000, -1.000000000000000000, 1.954868129030600086E-15 ) ) ;
#3271=DIRECTION ( 'NONE',  ( -0.9999862922474493931, -0.005235963827110273229, -0.000000000000000000 ) ) ;
#3285=PLANE ( 'NONE',  #22832 ) ;
#3339=CARTESIAN_POINT ( 'NONE',  ( -69.91240388362392366, 7.634045827809347706, 7.199999999999994849 ) ) ;
#3519=CARTESIAN_POINT ( 'NONE',  ( -69.82862846239015653, -8.365734848149525504, -7.200000000000000178 ) ) ;
#3789=ORIENTED_EDGE ( 'NONE', *, *, #15619, .F. ) ;
#3898=VERTEX_POINT ( 'NONE', #21903 ) ;
#4156=ADVANCED_FACE ( 'NONE', ( #17398 ), #6825, .T. ) ;
#4493=CARTESIAN_POINT ( 'NONE',  ( -69.91240388362392366, 7.634045827809356588, -7.200000000000000178 ) ) ;
#4511=ORIENTED_EDGE ( 'NONE', *, *, #4687, .F. ) ;
#4687=EDGE_CURVE ( 'NONE', #23033, #4801, #8337, .T. ) ;
#4787=VECTOR ( 'NONE', #3209, 1000.000000000000000 ) ;
#4801=VERTEX_POINT ( 'NONE', #14378 ) ;
#4848=EDGE_CURVE ( 'NONE', #10218, #23033, #21498, .T. ) ;
#4888=DIRECTION ( 'NONE',  ( -0.9999862922474493931, -0.005235963827116132258, -3.478334803857182996E-33 ) ) ;
#4990=CARTESIAN_POINT ( 'NONE',  ( -55.83667484026289429, -6.792351917569590114, -7.200000000000000178 ) ) ;
#5084=CARTESIAN_POINT ( 'NONE',  ( -55.83667431666650316, -6.792451916198809947, 7.200000000000000178 ) ) ;
#5194=LINE ( 'NONE', #12688, #21822 ) ;
#5341=PLANE ( 'NONE',  #3062 ) ;
#5512=CARTESIAN_POINT ( 'NONE',  ( -62.82872441665799101, -8.329083101359751495, -7.727128097349530051E-15 ) ) ;
#5707=SHAPE_REPRESENTATION_RELATIONSHIP ( 'NONE' , 'NONE' ,  #11914, #567 ) ;
#5754=CARTESIAN_POINT ( 'NONE',  ( -62.91249983789198552, 7.670697574599159907, -8.978560695896640676E-17 ) ) ;
#5802=EDGE_LOOP ( 'NONE', ( #16480, #3067, #3789, #21821 ) ) ;
#6111=AXIS2_PLACEMENT_3D ( 'NONE', #5754, #13012, #11005 ) ;
#6349=VERTEX_POINT ( 'NONE', #12733 ) ;
#6424=LINE ( 'NONE', #15339, #23147 ) ;
#6532=ORIENTED_EDGE ( 'NONE', *, *, #4848, .T. ) ;
#6825=PLANE ( 'NONE',  #11891 ) ;
#7016=ORIENTED_EDGE ( 'NONE', *, *, #12315, .F. ) ;
#7880=DIRECTION ( 'NONE',  ( -4.033639808943980242E-37, 5.936300330036069670E-19, -1.000000000000000000 ) ) ;
#8251=AXIS2_PLACEMENT_3D ( 'NONE', #5512, #12761, #7880 ) ;
#8259=VECTOR ( 'NONE', #4888, 1000.000000000000000 ) ;
#8337=LINE ( 'NONE', #15574, #2363 ) ;
#8591=CARTESIAN_POINT ( 'NONE',  ( -55.82882037092586813, -8.292431354569982815, 7.200000000000000178 ) ) ;
#8607=DIRECTION ( 'NONE',  ( 8.964882009398751025E-18, -1.954868129030600086E-15, -1.000000000000000000 ) ) ;
#8865=EDGE_CURVE ( 'NONE', #21144, #3898, #15860, .T. ) ;
#9016=ORIENTED_EDGE ( 'NONE', *, *, #11385, .F. ) ;
#9168=( NAMED_UNIT ( * ) SI_UNIT ( $, .STERADIAN. ) SOLID_ANGLE_UNIT ( ) );
#9294=ORIENTED_EDGE ( 'NONE', *, *, #18695, .F. ) ;
#9455=FACE_OUTER_BOUND ( 'NONE', #22455, .T. ) ;
#9683=PLANE ( 'NONE',  #8251 ) ;
#9853=EDGE_CURVE ( 'NONE', #23033, #1637, #6424, .T. ) ;
#10020=ADVANCED_FACE ( 'NONE', ( #16264 ), #5341, .T. ) ;
#10070=DIRECTION ( 'NONE',  ( -0.005235963827110212514, 0.9999862922474493931, 6.182393958678891872E-17 ) ) ;
#10218=VERTEX_POINT ( 'NONE', #2338 ) ;
#10428=CARTESIAN_POINT ( 'NONE',  ( -69.83648293172720400, -6.865655411149130138, 7.200000000000000178 ) ) ;
#10460=ADVANCED_FACE ( 'NONE', ( #1719 ), #12670, .T. ) ;
#10594=CLOSED_SHELL ( 'NONE', ( #10460, #20119, #20248, #10020, #4156, #1206 ) ) ;
#11005=DIRECTION ( 'NONE',  ( 5.034846547286470251E-14, -3.944250458554629736E-32, 1.000000000000000000 ) ) ;
#11251=ORIENTED_EDGE ( 'NONE', *, *, #12065, .F. ) ;
#11385=EDGE_CURVE ( 'NONE', #6349, #10218, #17365, .T. ) ;
#11887=AXIS2_PLACEMENT_3D ( 'NONE', #13138, #58, #16228 ) ;
#11891=AXIS2_PLACEMENT_3D ( 'NONE', #1338, #8607, #3248 ) ;
#11914=SHAPE_REPRESENTATION ( '1602p_c_25', ( #12739 ), #22737 ) ;
#12065=EDGE_CURVE ( 'NONE', #3898, #10218, #3159, .T. ) ;
#12139=PRODUCT_DEFINITION_SHAPE ( 'NONE', 'NONE',  #13468 ) ;
#12185=ORIENTED_EDGE ( 'NONE', *, *, #12315, .T. ) ;
#12289=CARTESIAN_POINT ( 'NONE',  ( -55.91259579215963527, 7.707349321388981878, -7.200000000000000178 ) ) ;
#12315=EDGE_CURVE ( 'NONE', #6349, #21144, #14201, .T. ) ;
#12384=DIRECTION ( 'NONE',  ( -1.380319151413309694E-18, 2.636191302913840582E-16, -1.000000000000000000 ) ) ;
#12486=CARTESIAN_POINT ( 'NONE',  ( -62.84171802989950351, -5.847508446296020068, 7.200000000000000178 ) ) ;
#12649=ORIENTED_EDGE ( 'NONE', *, *, #9853, .T. ) ;
#12670=PLANE ( 'NONE',  #6111 ) ;
#12688=CARTESIAN_POINT ( 'NONE',  ( -55.91259579215963527, 7.707349321388969443, 7.199999999999994849 ) ) ;
#12733=CARTESIAN_POINT ( 'NONE',  ( -55.91259579215963527, 7.707349321388969443, 7.200000000000000178 ) ) ;
#12739=AXIS2_PLACEMENT_3D ( 'NONE', #2569, #13380, #415 ) ;
#12761=DIRECTION ( 'NONE',  ( 0.005235963827110211646, -0.9999862922474493931, -5.936218956700079549E-19 ) ) ;
#12946=EDGE_LOOP ( 'NONE', ( #14258, #12185, #13528, #18427 ) ) ;
#13012=DIRECTION ( 'NONE',  ( -0.005235963827116131390, 0.9999862922474493931, 2.636227439667251184E-16 ) ) ;
#13019=EDGE_LOOP ( 'NONE', ( #3218, #9016, #16531, #22965 ) ) ;
#13138=CARTESIAN_POINT ( 'NONE',  ( -69.83648240813079155, -6.865755409778350860, -7.200000000000000178 ) ) ;
#13380=DIRECTION ( 'NONE',  ( 0.000000000000000000, 0.000000000000000000, 1.000000000000000000 ) ) ;
#13468=PRODUCT_DEFINITION ( 'UNKNOWN', '', #23156, #21325 ) ;
#13528=ORIENTED_EDGE ( 'NONE', *, *, #15619, .T. ) ;
#13536=MECHANICAL_CONTEXT ( 'NONE', #15179, 'mechanical' ) ;
#13809=DIRECTION ( 'NONE',  ( 0.005235963827110212514, -0.9999862922474493931, 1.836993535195700665E-15 ) ) ;
#13868=DIRECTION ( 'NONE',  ( 0.9999862922474493931, 0.005235963827110211646, 1.541976423090501796E-16 ) ) ;
#14004=ORIENTED_EDGE ( 'NONE', *, *, #2122, .F. ) ;
#14201=LINE ( 'NONE', #15972, #19650 ) ;
#14258=ORIENTED_EDGE ( 'NONE', *, *, #23416, .T. ) ;
#14369=DIRECTION ( 'NONE',  ( -3.974892857256893790E-34, -1.797095586565139883E-16, 1.000000000000000000 ) ) ;
#14378=CARTESIAN_POINT ( 'NONE',  ( -69.82862846239015653, -8.365734848149525504, -7.200000000000000178 ) ) ;
#14409=ORIENTED_EDGE ( 'NONE', *, *, #4687, .T. ) ;
#14412=ORIENTED_EDGE ( 'NONE', *, *, #14479, .T. ) ;
#14479=EDGE_CURVE ( 'NONE', #4801, #3898, #16756, .T. ) ;
#14693=LINE ( 'NONE', #20829, #1586 ) ;
#14982=DIRECTION ( 'NONE',  ( 3.108182772708750394E-21, -5.936137584479539905E-19, 1.000000000000000000 ) ) ;
#15179=APPLICATION_CONTEXT ( 'configuration controlled 3d designs of mechanical parts and assemblies' ) ;
#15339=CARTESIAN_POINT ( 'NONE',  ( -69.91240388362379576, 7.634045827809354812, -7.200000000000000178 ) ) ;
#15574=CARTESIAN_POINT ( 'NONE',  ( -69.82562477157480885, -8.939392295122029708, -7.200000000000000178 ) ) ;
#15619=EDGE_CURVE ( 'NONE', #21144, #23060, #14693, .T. ) ;
#15860=LINE ( 'NONE', #19544, #16453 ) ;
#15972=CARTESIAN_POINT ( 'NONE',  ( -55.82581668011050624, -8.866088801542479914, 7.200000000000000178 ) ) ;
#16228=DIRECTION ( 'NONE',  ( -0.005235963827110211646, 0.9999862922474493931, 0.000000000000000000 ) ) ;
#16264=FACE_OUTER_BOUND ( 'NONE', #22578, .T. ) ;
#16328=LINE ( 'NONE', #3519, #20955 ) ;
#16453=VECTOR ( 'NONE', #3271, 1000.000000000000114 ) ;
#16480=ORIENTED_EDGE ( 'NONE', *, *, #14479, .F. ) ;
#16531=ORIENTED_EDGE ( 'NONE', *, *, #23416, .F. ) ;
#16596=CARTESIAN_POINT ( 'NONE',  ( -55.82882037092586813, -8.292431354569982815, -7.200000000000000178 ) ) ;
#16604=VECTOR ( 'NONE', #10070, 1000.000000000000000 ) ;
#16665=VECTOR ( 'NONE', #12384, 1000.000000000000000 ) ;
#16756=LINE ( 'NONE', #20331, #1392 ) ;
#17365=LINE ( 'NONE', #22928, #8259 ) ;
#17398=FACE_OUTER_BOUND ( 'NONE', #18630, .T. ) ;
#17556=FACE_OUTER_BOUND ( 'NONE', #12946, .T. ) ;
#18055=DIRECTION ( 'NONE',  ( 1.000000000000000000, -2.211842757264940144E-18, 0.000000000000000000 ) ) ;
#18427=ORIENTED_EDGE ( 'NONE', *, *, #2122, .T. ) ;
#18463=FACE_OUTER_BOUND ( 'NONE', #5802, .T. ) ;
#18630=EDGE_LOOP ( 'NONE', ( #4511, #12649, #14004, #9294 ) ) ;
#18695=EDGE_CURVE ( 'NONE', #4801, #23060, #16328, .T. ) ;
#19040=ORIENTED_EDGE ( 'NONE', *, *, #12065, .T. ) ;
#19544=CARTESIAN_POINT ( 'NONE',  ( -69.82862846239015653, -8.365734848149525504, 7.200000000000000178 ) ) ;
#19650=VECTOR ( 'NONE', #19772, 1000.000000000000000 ) ;
#19708=LINE ( 'NONE', #4990, #4787 ) ;
#19772=DIRECTION ( 'NONE',  ( 0.005235963827110212514, -0.9999862922474493931, -6.182393958678891872E-17 ) ) ;
#20097=UNCERTAINTY_MEASURE_WITH_UNIT (LENGTH_MEASURE( 1.000000000000000082E-05 ), #2396, 'distance_accuracy_value', 'NONE');
#20119=ADVANCED_FACE ( 'NONE', ( #17556 ), #3285, .T. ) ;
#20248=ADVANCED_FACE ( 'NONE', ( #9455 ), #21674, .T. ) ;
#20331=CARTESIAN_POINT ( 'NONE',  ( -69.82862846239019916, -8.365734848149529057, -7.200000000000000178 ) ) ;
#20829=CARTESIAN_POINT ( 'NONE',  ( -55.82882037092589655, -8.292431354569981039, 7.200000000000000178 ) ) ;
#20955=VECTOR ( 'NONE', #52, 1000.000000000000114 ) ;
#21100=DIRECTION ( 'NONE',  ( 0.000000000000000000, 2.944971497141790110E-14, -1.000000000000000000 ) ) ;
#21144=VERTEX_POINT ( 'NONE', #8591 ) ;
#21325=DESIGN_CONTEXT ( 'detailed design', #21752, 'design' ) ;
#21460=DIRECTION ( 'NONE',  ( 1.380319151413309694E-18, -2.636191302913840582E-16, 1.000000000000000000 ) ) ;
#21498=LINE ( 'NONE', #3339, #16665 ) ;
#21674=PLANE ( 'NONE',  #11887 ) ;
#21752=APPLICATION_CONTEXT ( 'configuration controlled 3d designs of mechanical parts and assemblies' ) ;
#21821=ORIENTED_EDGE ( 'NONE', *, *, #8865, .T. ) ;
#21822=VECTOR ( 'NONE', #21460, 1000.000000000000000 ) ;
#21903=CARTESIAN_POINT ( 'NONE',  ( -69.82862846239015653, -8.365734848149525504, 7.200000000000000178 ) ) ;
#21926=DIRECTION ( 'NONE',  ( 1.541924204231519956E-16, 1.400987035803820065E-18, -1.000000000000000000 ) ) ;
#22455=EDGE_LOOP ( 'NONE', ( #19040, #6532, #14409, #14412 ) ) ;
#22567=DIRECTION ( 'NONE',  ( 0.9999862922474493931, 0.005235963827116132258, 3.478334803857182996E-33 ) ) ;
#22578=EDGE_LOOP ( 'NONE', ( #7016, #23280, #11251, #1752 ) ) ;
#22737=( GEOMETRIC_REPRESENTATION_CONTEXT ( 3 ) GLOBAL_UNCERTAINTY_ASSIGNED_CONTEXT ( ( #20097 ) ) GLOBAL_UNIT_ASSIGNED_CONTEXT ( ( #2396, #1909, #9168 ) ) REPRESENTATION_CONTEXT ( 'NONE', 'WORKASPACE' ) );
#22832=AXIS2_PLACEMENT_3D ( 'NONE', #5084, #13868, #21100 ) ;
#22928=CARTESIAN_POINT ( 'NONE',  ( -69.91240388362379576, 7.634045827809347706, 7.200000000000000178 ) ) ;
#22965=ORIENTED_EDGE ( 'NONE', *, *, #9853, .F. ) ;
#23033=VERTEX_POINT ( 'NONE', #4493 ) ;
#23060=VERTEX_POINT ( 'NONE', #16596 ) ;
#23147=VECTOR ( 'NONE', #22567, 1000.000000000000000 ) ;
#23156=PRODUCT_DEFINITION_FORMATION_WITH_SPECIFIED_SOURCE ( 'ANY', '', #1883, .NOT_KNOWN. ) ;
#23280=ORIENTED_EDGE ( 'NONE', *, *, #11385, .T. ) ;
#23416=EDGE_CURVE ( 'NONE', #1637, #6349, #5194, .T. ) ;
#23515=COLOUR_RGB('Deep Blue', 0.09019608, 0.27058824, 0.51372549);
#23516=FILL_AREA_STYLE_COLOUR('',#23515);
#23517=FILL_AREA_STYLE('',(#23516));
#23518=SURFACE_STYLE_FILL_AREA(#23517);
#23519=SURFACE_SIDE_STYLE('',(#23518));
#23520=SURFACE_STYLE_USAGE(.BOTH.,#23519);
#23521=PRESENTATION_STYLE_ASSIGNMENT((#23520));
#23557=STYLED_ITEM('',(#23521),#1705);
#23558=MECHANICAL_DESIGN_GEOMETRIC_PRESENTATION_REPRESENTATION('',(#23557),#22737);
ENDSEC;
END-ISO-10303-21;
